ISO-10303-21;
HEADER;
/* Generated by software containing ST-Developer
 * from STEP Tools, Inc. (www.steptools.com) 
 */

FILE_DESCRIPTION(
/* description */ ('Single-Axis Profile-Rail Linear Slide'),
/* implementation_level */ '2;1');

FILE_NAME(
/* name */ 'Cap Screw - M6x25.step',
/* time_stamp */ '2026-10-27T10:47:43-07:00',
/* author */ (''),
/* organization */ (''),
/* preprocessor_version */ 'ST-DEVELOPER v20.2',
/* originating_system */ 'Autodesk Translation Framework v15.17.0.0',
/* authorisation */ '');

FILE_SCHEMA (('AUTOMOTIVE_DESIGN { 1 0 10303 214 3 1 1 }'));
ENDSEC;

DATA;
#10=MECHANICAL_DESIGN_GEOMETRIC_PRESENTATION_REPRESENTATION('',(#355),#14478);
#259=CONICAL_SURFACE('',#9580,0.475,0.785398163397449);
#260=CONICAL_SURFACE('',#9584,0.485,0.785398163397448);
#261=CONICAL_SURFACE('',#9588,0.31,0.463647609000806);
#262=CONICAL_SURFACE('',#9592,0.27,0.785398163397448);
#267=ORIENTED_CLOSED_SHELL('',*,#8620,.F.);
#272=BREP_WITH_VOIDS('Body1',#8619,(#267));
#301=SHAPE_REPRESENTATION_RELATIONSHIP('SRR','None',#14633,#328);
#328=ADVANCED_BREP_SHAPE_REPRESENTATION('',(#272),#14477);
#355=STYLED_ITEM('',(#14838),#272);
#467=FACE_BOUND('',#1827,.T.);
#829=PLANE('',#9578);
#830=PLANE('',#9586);
#831=PLANE('',#9594);
#832=PLANE('',#9595);
#833=PLANE('',#9596);
#834=PLANE('',#9597);
#835=PLANE('',#9598);
#836=PLANE('',#9599);
#837=PLANE('',#9600);
#838=PLANE('',#9601);
#839=PLANE('',#9602);
#1278=FACE_OUTER_BOUND('',#1822,.T.);
#1279=FACE_OUTER_BOUND('',#1823,.T.);
#1280=FACE_OUTER_BOUND('',#1824,.T.);
#1281=FACE_OUTER_BOUND('',#1825,.T.);
#1282=FACE_OUTER_BOUND('',#1826,.T.);
#1283=FACE_OUTER_BOUND('',#1828,.T.);
#1284=FACE_OUTER_BOUND('',#1829,.T.);
#1285=FACE_OUTER_BOUND('',#1830,.T.);
#1286=FACE_OUTER_BOUND('',#1831,.T.);
#1287=FACE_OUTER_BOUND('',#1832,.T.);
#1288=FACE_OUTER_BOUND('',#1833,.T.);
#1289=FACE_OUTER_BOUND('',#1834,.T.);
#1290=FACE_OUTER_BOUND('',#1835,.T.);
#1291=FACE_OUTER_BOUND('',#1836,.T.);
#1292=FACE_OUTER_BOUND('',#1837,.T.);
#1293=FACE_OUTER_BOUND('',#1838,.T.);
#1294=FACE_OUTER_BOUND('',#1839,.T.);
#1822=EDGE_LOOP('',(#8007));
#1823=EDGE_LOOP('',(#8008,#8009,#8010,#8011));
#1824=EDGE_LOOP('',(#8012,#8013,#8014,#8015));
#1825=EDGE_LOOP('',(#8016,#8017,#8018,#8019));
#1826=EDGE_LOOP('',(#8020));
#1827=EDGE_LOOP('',(#8021));
#1828=EDGE_LOOP('',(#8022,#8023,#8024,#8025));
#1829=EDGE_LOOP('',(#8026,#8027,#8028,#8029));
#1830=EDGE_LOOP('',(#8030,#8031,#8032,#8033));
#1831=EDGE_LOOP('',(#8034));
#1832=EDGE_LOOP('',(#8035,#8036,#8037,#8038));
#1833=EDGE_LOOP('',(#8039,#8040,#8041,#8042));
#1834=EDGE_LOOP('',(#8043,#8044,#8045,#8046));
#1835=EDGE_LOOP('',(#8047,#8048,#8049,#8050));
#1836=EDGE_LOOP('',(#8051,#8052,#8053,#8054));
#1837=EDGE_LOOP('',(#8055,#8056,#8057,#8058));
#1838=EDGE_LOOP('',(#8059,#8060,#8061,#8062,#8063,#8064));
#1839=EDGE_LOOP('',(#8065,#8066,#8067,#8068,#8069,#8070));
#2787=LINE('',#14334,#3758);
#2788=LINE('',#14338,#3759);
#2789=LINE('',#14342,#3760);
#2790=LINE('',#14349,#3761);
#2791=LINE('',#14353,#3762);
#2792=LINE('',#14357,#3763);
#2793=LINE('',#14362,#3764);
#2794=LINE('',#14364,#3765);
#2795=LINE('',#14366,#3766);
#2796=LINE('',#14367,#3767);
#2797=LINE('',#14370,#3768);
#2798=LINE('',#14372,#3769);
#2799=LINE('',#14373,#3770);
#2800=LINE('',#14376,#3771);
#2801=LINE('',#14378,#3772);
#2802=LINE('',#14379,#3773);
#2803=LINE('',#14382,#3774);
#2804=LINE('',#14384,#3775);
#2805=LINE('',#14385,#3776);
#2806=LINE('',#14388,#3777);
#2807=LINE('',#14390,#3778);
#2808=LINE('',#14391,#3779);
#2809=LINE('',#14393,#3780);
#2810=LINE('',#14394,#3781);
#3758=VECTOR('',#11894,0.475);
#3759=VECTOR('',#11899,0.5);
#3760=VECTOR('',#11904,0.485);
#3761=VECTOR('',#11913,0.31);
#3762=VECTOR('',#11918,0.3);
#3763=VECTOR('',#11923,0.27);
#3764=VECTOR('',#11928,1.);
#3765=VECTOR('',#11929,1.);
#3766=VECTOR('',#11930,1.);
#3767=VECTOR('',#11931,1.);
#3768=VECTOR('',#11934,1.);
#3769=VECTOR('',#11935,1.);
#3770=VECTOR('',#11936,1.);
#3771=VECTOR('',#11939,1.);
#3772=VECTOR('',#11940,1.);
#3773=VECTOR('',#11941,1.);
#3774=VECTOR('',#11944,1.);
#3775=VECTOR('',#11945,1.);
#3776=VECTOR('',#11946,1.);
#3777=VECTOR('',#11949,1.);
#3778=VECTOR('',#11950,1.);
#3779=VECTOR('',#11951,1.);
#3780=VECTOR('',#11954,1.);
#3781=VECTOR('',#11955,1.);
#3930=CIRCLE('',#9579,0.45);
#3931=CIRCLE('',#9581,0.5);
#3932=CIRCLE('',#9583,0.5);
#3933=CIRCLE('',#9585,0.47);
#3934=CIRCLE('',#9587,0.32);
#3935=CIRCLE('',#9589,0.2942);
#3936=CIRCLE('',#9591,0.2942);
#3937=CIRCLE('',#9593,0.24);
#4664=VERTEX_POINT('',#14329);
#4665=VERTEX_POINT('',#14332);
#4666=VERTEX_POINT('',#14336);
#4667=VERTEX_POINT('',#14340);
#4668=VERTEX_POINT('',#14344);
#4669=VERTEX_POINT('',#14347);
#4670=VERTEX_POINT('',#14351);
#4671=VERTEX_POINT('',#14355);
#4672=VERTEX_POINT('',#14360);
#4673=VERTEX_POINT('',#14361);
#4674=VERTEX_POINT('',#14363);
#4675=VERTEX_POINT('',#14365);
#4676=VERTEX_POINT('',#14369);
#4677=VERTEX_POINT('',#14371);
#4678=VERTEX_POINT('',#14375);
#4679=VERTEX_POINT('',#14377);
#4680=VERTEX_POINT('',#14381);
#4681=VERTEX_POINT('',#14383);
#4682=VERTEX_POINT('',#14387);
#4683=VERTEX_POINT('',#14389);
#5781=EDGE_CURVE('',#4664,#4664,#3930,.T.);
#5782=EDGE_CURVE('',#4665,#4665,#3931,.T.);
#5783=EDGE_CURVE('',#4665,#4664,#2787,.T.);
#5784=EDGE_CURVE('',#4666,#4666,#3932,.T.);
#5785=EDGE_CURVE('',#4666,#4665,#2788,.T.);
#5786=EDGE_CURVE('',#4667,#4667,#3933,.T.);
#5787=EDGE_CURVE('',#4667,#4666,#2789,.T.);
#5788=EDGE_CURVE('',#4668,#4668,#3934,.T.);
#5789=EDGE_CURVE('',#4669,#4669,#3935,.F.);
#5790=EDGE_CURVE('',#4669,#4668,#2790,.T.);
#5791=EDGE_CURVE('',#4670,#4670,#3936,.F.);
#5792=EDGE_CURVE('',#4670,#4669,#2791,.T.);
#5793=EDGE_CURVE('',#4671,#4671,#3937,.T.);
#5794=EDGE_CURVE('',#4671,#4670,#2792,.T.);
#5795=EDGE_CURVE('',#4672,#4673,#2793,.T.);
#5796=EDGE_CURVE('',#4673,#4674,#2794,.T.);
#5797=EDGE_CURVE('',#4674,#4675,#2795,.T.);
#5798=EDGE_CURVE('',#4672,#4675,#2796,.T.);
#5799=EDGE_CURVE('',#4673,#4676,#2797,.T.);
#5800=EDGE_CURVE('',#4676,#4677,#2798,.T.);
#5801=EDGE_CURVE('',#4677,#4674,#2799,.T.);
#5802=EDGE_CURVE('',#4676,#4678,#2800,.T.);
#5803=EDGE_CURVE('',#4678,#4679,#2801,.T.);
#5804=EDGE_CURVE('',#4679,#4677,#2802,.T.);
#5805=EDGE_CURVE('',#4678,#4680,#2803,.T.);
#5806=EDGE_CURVE('',#4680,#4681,#2804,.T.);
#5807=EDGE_CURVE('',#4681,#4679,#2805,.T.);
#5808=EDGE_CURVE('',#4680,#4682,#2806,.T.);
#5809=EDGE_CURVE('',#4682,#4683,#2807,.T.);
#5810=EDGE_CURVE('',#4683,#4681,#2808,.T.);
#5811=EDGE_CURVE('',#4682,#4672,#2809,.T.);
#5812=EDGE_CURVE('',#4675,#4683,#2810,.T.);
#8007=ORIENTED_EDGE('',*,*,#5781,.F.);
#8008=ORIENTED_EDGE('',*,*,#5782,.F.);
#8009=ORIENTED_EDGE('',*,*,#5783,.T.);
#8010=ORIENTED_EDGE('',*,*,#5781,.T.);
#8011=ORIENTED_EDGE('',*,*,#5783,.F.);
#8012=ORIENTED_EDGE('',*,*,#5784,.F.);
#8013=ORIENTED_EDGE('',*,*,#5785,.T.);
#8014=ORIENTED_EDGE('',*,*,#5782,.T.);
#8015=ORIENTED_EDGE('',*,*,#5785,.F.);
#8016=ORIENTED_EDGE('',*,*,#5786,.F.);
#8017=ORIENTED_EDGE('',*,*,#5787,.T.);
#8018=ORIENTED_EDGE('',*,*,#5784,.T.);
#8019=ORIENTED_EDGE('',*,*,#5787,.F.);
#8020=ORIENTED_EDGE('',*,*,#5786,.T.);
#8021=ORIENTED_EDGE('',*,*,#5788,.F.);
#8022=ORIENTED_EDGE('',*,*,#5789,.F.);
#8023=ORIENTED_EDGE('',*,*,#5790,.T.);
#8024=ORIENTED_EDGE('',*,*,#5788,.T.);
#8025=ORIENTED_EDGE('',*,*,#5790,.F.);
#8026=ORIENTED_EDGE('',*,*,#5791,.F.);
#8027=ORIENTED_EDGE('',*,*,#5792,.T.);
#8028=ORIENTED_EDGE('',*,*,#5789,.T.);
#8029=ORIENTED_EDGE('',*,*,#5792,.F.);
#8030=ORIENTED_EDGE('',*,*,#5793,.F.);
#8031=ORIENTED_EDGE('',*,*,#5794,.T.);
#8032=ORIENTED_EDGE('',*,*,#5791,.T.);
#8033=ORIENTED_EDGE('',*,*,#5794,.F.);
#8034=ORIENTED_EDGE('',*,*,#5793,.T.);
#8035=ORIENTED_EDGE('',*,*,#5795,.T.);
#8036=ORIENTED_EDGE('',*,*,#5796,.T.);
#8037=ORIENTED_EDGE('',*,*,#5797,.T.);
#8038=ORIENTED_EDGE('',*,*,#5798,.F.);
#8039=ORIENTED_EDGE('',*,*,#5799,.T.);
#8040=ORIENTED_EDGE('',*,*,#5800,.T.);
#8041=ORIENTED_EDGE('',*,*,#5801,.T.);
#8042=ORIENTED_EDGE('',*,*,#5796,.F.);
#8043=ORIENTED_EDGE('',*,*,#5802,.T.);
#8044=ORIENTED_EDGE('',*,*,#5803,.T.);
#8045=ORIENTED_EDGE('',*,*,#5804,.T.);
#8046=ORIENTED_EDGE('',*,*,#5800,.F.);
#8047=ORIENTED_EDGE('',*,*,#5805,.T.);
#8048=ORIENTED_EDGE('',*,*,#5806,.T.);
#8049=ORIENTED_EDGE('',*,*,#5807,.T.);
#8050=ORIENTED_EDGE('',*,*,#5803,.F.);
#8051=ORIENTED_EDGE('',*,*,#5808,.T.);
#8052=ORIENTED_EDGE('',*,*,#5809,.T.);
#8053=ORIENTED_EDGE('',*,*,#5810,.T.);
#8054=ORIENTED_EDGE('',*,*,#5806,.F.);
#8055=ORIENTED_EDGE('',*,*,#5811,.T.);
#8056=ORIENTED_EDGE('',*,*,#5798,.T.);
#8057=ORIENTED_EDGE('',*,*,#5812,.T.);
#8058=ORIENTED_EDGE('',*,*,#5809,.F.);
#8059=ORIENTED_EDGE('',*,*,#5811,.F.);
#8060=ORIENTED_EDGE('',*,*,#5808,.F.);
#8061=ORIENTED_EDGE('',*,*,#5805,.F.);
#8062=ORIENTED_EDGE('',*,*,#5802,.F.);
#8063=ORIENTED_EDGE('',*,*,#5799,.F.);
#8064=ORIENTED_EDGE('',*,*,#5795,.F.);
#8065=ORIENTED_EDGE('',*,*,#5812,.F.);
#8066=ORIENTED_EDGE('',*,*,#5797,.F.);
#8067=ORIENTED_EDGE('',*,*,#5801,.F.);
#8068=ORIENTED_EDGE('',*,*,#5804,.F.);
#8069=ORIENTED_EDGE('',*,*,#5807,.F.);
#8070=ORIENTED_EDGE('',*,*,#5810,.F.);
#8132=CYLINDRICAL_SURFACE('',#9582,0.5);
#8133=CYLINDRICAL_SURFACE('',#9590,0.2942);
#8572=ADVANCED_FACE('',(#1278),#829,.T.);
#8573=ADVANCED_FACE('',(#1279),#259,.T.);
#8574=ADVANCED_FACE('',(#1280),#8132,.T.);
#8575=ADVANCED_FACE('',(#1281),#260,.T.);
#8576=ADVANCED_FACE('',(#1282,#467),#830,.T.);
#8577=ADVANCED_FACE('',(#1283),#261,.T.);
#8578=ADVANCED_FACE('',(#1284),#8133,.T.);
#8579=ADVANCED_FACE('',(#1285),#262,.T.);
#8580=ADVANCED_FACE('',(#1286),#831,.T.);
#8581=ADVANCED_FACE('',(#1287),#832,.F.);
#8582=ADVANCED_FACE('',(#1288),#833,.F.);
#8583=ADVANCED_FACE('',(#1289),#834,.F.);
#8584=ADVANCED_FACE('',(#1290),#835,.F.);
#8585=ADVANCED_FACE('',(#1291),#836,.F.);
#8586=ADVANCED_FACE('',(#1292),#837,.F.);
#8587=ADVANCED_FACE('',(#1293),#838,.F.);
#8588=ADVANCED_FACE('',(#1294),#839,.F.);
#8619=CLOSED_SHELL('',(#8572,#8573,#8574,#8575,#8576,#8577,#8578,#8579,
#8580));
#8620=CLOSED_SHELL('',(#8581,#8582,#8583,#8584,#8585,#8586,#8587,#8588));
#9577=AXIS2_PLACEMENT_3D('',#14327,#11884,#11885);
#9578=AXIS2_PLACEMENT_3D('',#14328,#11886,#11887);
#9579=AXIS2_PLACEMENT_3D('',#14330,#11888,#11889);
#9580=AXIS2_PLACEMENT_3D('',#14331,#11890,#11891);
#9581=AXIS2_PLACEMENT_3D('',#14333,#11892,#11893);
#9582=AXIS2_PLACEMENT_3D('',#14335,#11895,#11896);
#9583=AXIS2_PLACEMENT_3D('',#14337,#11897,#11898);
#9584=AXIS2_PLACEMENT_3D('',#14339,#11900,#11901);
#9585=AXIS2_PLACEMENT_3D('',#14341,#11902,#11903);
#9586=AXIS2_PLACEMENT_3D('',#14343,#11905,#11906);
#9587=AXIS2_PLACEMENT_3D('',#14345,#11907,#11908);
#9588=AXIS2_PLACEMENT_3D('',#14346,#11909,#11910);
#9589=AXIS2_PLACEMENT_3D('',#14348,#11911,#11912);
#9590=AXIS2_PLACEMENT_3D('',#14350,#11914,#11915);
#9591=AXIS2_PLACEMENT_3D('',#14352,#11916,#11917);
#9592=AXIS2_PLACEMENT_3D('',#14354,#11919,#11920);
#9593=AXIS2_PLACEMENT_3D('',#14356,#11921,#11922);
#9594=AXIS2_PLACEMENT_3D('',#14358,#11924,#11925);
#9595=AXIS2_PLACEMENT_3D('',#14359,#11926,#11927);
#9596=AXIS2_PLACEMENT_3D('',#14368,#11932,#11933);
#9597=AXIS2_PLACEMENT_3D('',#14374,#11937,#11938);
#9598=AXIS2_PLACEMENT_3D('',#14380,#11942,#11943);
#9599=AXIS2_PLACEMENT_3D('',#14386,#11947,#11948);
#9600=AXIS2_PLACEMENT_3D('',#14392,#11952,#11953);
#9601=AXIS2_PLACEMENT_3D('',#14395,#11956,#11957);
#9602=AXIS2_PLACEMENT_3D('',#14396,#11958,#11959);
#11884=DIRECTION('axis',(0.,0.,1.));
#11885=DIRECTION('refdir',(1.,0.,0.));
#11886=DIRECTION('center_axis',(0.,1.,0.));
#11887=DIRECTION('ref_axis',(0.,0.,1.));
#11888=DIRECTION('center_axis',(0.,-1.,0.));
#11889=DIRECTION('ref_axis',(1.,0.,0.));
#11890=DIRECTION('center_axis',(0.,-1.,0.));
#11891=DIRECTION('ref_axis',(1.,0.,0.));
#11892=DIRECTION('center_axis',(0.,-1.,0.));
#11893=DIRECTION('ref_axis',(1.,0.,0.));
#11894=DIRECTION('',(0.707106781186548,0.707106781186547,8.65956056235494E-17));
#11895=DIRECTION('center_axis',(0.,-1.,0.));
#11896=DIRECTION('ref_axis',(1.,0.,0.));
#11897=DIRECTION('center_axis',(0.,-1.,0.));
#11898=DIRECTION('ref_axis',(1.,0.,0.));
#11899=DIRECTION('',(0.,1.,0.));
#11900=DIRECTION('center_axis',(0.,1.,0.));
#11901=DIRECTION('ref_axis',(1.,0.,0.));
#11902=DIRECTION('center_axis',(0.,-1.,0.));
#11903=DIRECTION('ref_axis',(1.,0.,0.));
#11904=DIRECTION('',(-0.707106781186547,0.707106781186548,-8.65956056235493E-17));
#11905=DIRECTION('center_axis',(0.,-1.,0.));
#11906=DIRECTION('ref_axis',(0.,0.,-1.));
#11907=DIRECTION('center_axis',(0.,-1.,0.));
#11908=DIRECTION('ref_axis',(1.,0.,0.));
#11909=DIRECTION('center_axis',(0.,1.,0.));
#11910=DIRECTION('ref_axis',(1.,0.,0.));
#11911=DIRECTION('center_axis',(0.,1.,0.));
#11912=DIRECTION('ref_axis',(1.,0.,0.));
#11913=DIRECTION('',(-0.447213595499958,0.894427190999916,-5.47678698264203E-17));
#11914=DIRECTION('center_axis',(0.,-1.,0.));
#11915=DIRECTION('ref_axis',(1.,0.,0.));
#11916=DIRECTION('center_axis',(0.,1.,0.));
#11917=DIRECTION('ref_axis',(1.,0.,0.));
#11918=DIRECTION('',(0.,1.,0.));
#11919=DIRECTION('center_axis',(0.,1.,0.));
#11920=DIRECTION('ref_axis',(1.,0.,0.));
#11921=DIRECTION('center_axis',(0.,-1.,0.));
#11922=DIRECTION('ref_axis',(1.,0.,0.));
#11923=DIRECTION('',(-0.707106781186547,0.707106781186548,-8.65956056235493E-17));
#11924=DIRECTION('center_axis',(0.,-1.,0.));
#11925=DIRECTION('ref_axis',(0.,0.,-1.));
#11926=DIRECTION('center_axis',(0.866025403784439,0.,-0.5));
#11927=DIRECTION('ref_axis',(0.5,0.,0.866025403784439));
#11928=DIRECTION('',(-0.5,0.,-0.866025403784439));
#11929=DIRECTION('',(0.,-1.,0.));
#11930=DIRECTION('',(0.5,0.,0.866025403784439));
#11931=DIRECTION('',(0.,-1.,0.));
#11932=DIRECTION('center_axis',(1.92296268638356E-16,0.,-1.));
#11933=DIRECTION('ref_axis',(1.,0.,1.92296268638356E-16));
#11934=DIRECTION('',(-1.,0.,-1.92296268638356E-16));
#11935=DIRECTION('',(0.,-1.,0.));
#11936=DIRECTION('',(1.,0.,1.92296268638356E-16));
#11937=DIRECTION('center_axis',(-0.866025403784439,0.,-0.5));
#11938=DIRECTION('ref_axis',(0.5,0.,-0.866025403784439));
#11939=DIRECTION('',(-0.5,0.,0.866025403784438));
#11940=DIRECTION('',(0.,-1.,0.));
#11941=DIRECTION('',(0.5,0.,-0.866025403784438));
#11942=DIRECTION('center_axis',(-0.866025403784439,0.,0.5));
#11943=DIRECTION('ref_axis',(-0.5,0.,-0.866025403784439));
#11944=DIRECTION('',(0.5,0.,0.866025403784439));
#11945=DIRECTION('',(0.,-1.,0.));
#11946=DIRECTION('',(-0.5,0.,-0.866025403784439));
#11947=DIRECTION('center_axis',(-1.92296268638356E-16,0.,1.));
#11948=DIRECTION('ref_axis',(-1.,0.,-1.92296268638356E-16));
#11949=DIRECTION('',(1.,0.,1.92296268638356E-16));
#11950=DIRECTION('',(0.,-1.,0.));
#11951=DIRECTION('',(-1.,0.,-1.92296268638356E-16));
#11952=DIRECTION('center_axis',(0.866025403784439,0.,0.5));
#11953=DIRECTION('ref_axis',(-0.5,0.,0.866025403784439));
#11954=DIRECTION('',(0.5,0.,-0.866025403784439));
#11955=DIRECTION('',(-0.5,0.,0.866025403784439));
#11956=DIRECTION('center_axis',(0.,1.,0.));
#11957=DIRECTION('ref_axis',(1.,0.,0.));
#11958=DIRECTION('center_axis',(0.,-1.,0.));
#11959=DIRECTION('ref_axis',(0.,0.,-1.));
#14327=CARTESIAN_POINT('',(0.,0.,0.));
#14328=CARTESIAN_POINT('Origin',(0.45,0.6,0.));
#14329=CARTESIAN_POINT('',(-0.45,0.6,-5.51091059616309E-17));
#14330=CARTESIAN_POINT('Origin',(0.,0.6,0.));
#14331=CARTESIAN_POINT('Origin',(0.,0.575,0.));
#14332=CARTESIAN_POINT('',(-0.5,0.55,-6.12323399573677E-17));
#14333=CARTESIAN_POINT('Origin',(0.,0.55,0.));
#14334=CARTESIAN_POINT('',(-0.475,0.575,-5.81707229594993E-17));
#14335=CARTESIAN_POINT('Origin',(0.,0.29,0.));
#14336=CARTESIAN_POINT('',(-0.5,0.0299999999999998,-6.12323399573677E-17));
#14337=CARTESIAN_POINT('Origin',(0.,0.0299999999999998,0.));
#14338=CARTESIAN_POINT('',(-0.5,0.29,-6.12323399573677E-17));
#14339=CARTESIAN_POINT('Origin',(0.,0.0150000000000001,0.));
#14340=CARTESIAN_POINT('',(-0.47,7.11236625150491E-17,-5.75583995599256E-17));
#14341=CARTESIAN_POINT('Origin',(0.,0.,0.));
#14342=CARTESIAN_POINT('',(-0.485,0.0150000000000001,-5.93953697586466E-17));
#14343=CARTESIAN_POINT('Origin',(0.32,0.,0.));
#14344=CARTESIAN_POINT('',(-0.32,-6.93889390390723E-18,-3.91886975727153E-17));
#14345=CARTESIAN_POINT('Origin',(0.,0.,0.));
#14346=CARTESIAN_POINT('Origin',(0.,-0.02,0.));
#14347=CARTESIAN_POINT('',(-0.2942,-0.0515999999999999,3.60291088309151E-17));
#14348=CARTESIAN_POINT('Origin',(0.,-0.0515999999999999,0.));
#14349=CARTESIAN_POINT('',(-0.31,-0.02,-3.7964050773568E-17));
#14350=CARTESIAN_POINT('Origin',(0.,-1.24,0.));
#14351=CARTESIAN_POINT('',(-0.2942,-2.4458,3.60291088309151E-17));
#14352=CARTESIAN_POINT('Origin',(0.,-2.4458,0.));
#14353=CARTESIAN_POINT('',(-0.2942,-1.24,-3.60291088309151E-17));
#14354=CARTESIAN_POINT('Origin',(0.,-2.47,0.));
#14355=CARTESIAN_POINT('',(-0.24,-2.5,-2.93915231795365E-17));
#14356=CARTESIAN_POINT('Origin',(0.,-2.5,0.));
#14357=CARTESIAN_POINT('',(-0.27,-2.47,-3.30654635769785E-17));
#14358=CARTESIAN_POINT('Origin',(0.,-2.5,0.));
#14359=CARTESIAN_POINT('Origin',(0.144337567297406,-0.6,-0.25));
#14360=CARTESIAN_POINT('',(0.288675134594813,-0.6,0.));
#14361=CARTESIAN_POINT('',(0.144337567297406,-0.6,-0.25));
#14362=CARTESIAN_POINT('',(0.288675134594813,-0.6,0.));
#14363=CARTESIAN_POINT('',(0.144337567297406,-0.96,-0.25));
#14364=CARTESIAN_POINT('',(0.144337567297406,-0.6,-0.25));
#14365=CARTESIAN_POINT('',(0.288675134594813,-0.96,0.));
#14366=CARTESIAN_POINT('',(0.288675134594813,-0.96,0.));
#14367=CARTESIAN_POINT('',(0.288675134594813,-0.6,0.));
#14368=CARTESIAN_POINT('Origin',(-0.144337567297406,-0.6,-0.25));
#14369=CARTESIAN_POINT('',(-0.144337567297406,-0.6,-0.25));
#14370=CARTESIAN_POINT('',(0.144337567297406,-0.6,-0.25));
#14371=CARTESIAN_POINT('',(-0.144337567297406,-0.96,-0.25));
#14372=CARTESIAN_POINT('',(-0.144337567297406,-0.6,-0.25));
#14373=CARTESIAN_POINT('',(0.144337567297406,-0.96,-0.25));
#14374=CARTESIAN_POINT('Origin',(-0.288675134594813,-0.6,-8.32667268468867E-17));
#14375=CARTESIAN_POINT('',(-0.288675134594813,-0.6,-3.53525079574969E-17));
#14376=CARTESIAN_POINT('',(-0.144337567297406,-0.6,-0.25));
#14377=CARTESIAN_POINT('',(-0.288675134594813,-0.96,-5.55111512312578E-17));
#14378=CARTESIAN_POINT('',(-0.288675134594813,-0.6,-3.53525079574969E-17));
#14379=CARTESIAN_POINT('',(-0.144337567297406,-0.96,-0.25));
#14380=CARTESIAN_POINT('Origin',(-0.144337567297407,-0.6,0.25));
#14381=CARTESIAN_POINT('',(-0.144337567297407,-0.6,0.25));
#14382=CARTESIAN_POINT('',(-0.288675134594813,-0.6,-3.53525079574969E-17));
#14383=CARTESIAN_POINT('',(-0.144337567297407,-0.96,0.25));
#14384=CARTESIAN_POINT('',(-0.144337567297407,-0.6,0.25));
#14385=CARTESIAN_POINT('',(-0.288675134594813,-0.96,-3.53525079574969E-17));
#14386=CARTESIAN_POINT('Origin',(0.144337567297406,-0.6,0.25));
#14387=CARTESIAN_POINT('',(0.144337567297406,-0.6,0.25));
#14388=CARTESIAN_POINT('',(-0.144337567297407,-0.6,0.25));
#14389=CARTESIAN_POINT('',(0.144337567297406,-0.96,0.25));
#14390=CARTESIAN_POINT('',(0.144337567297406,-0.6,0.25));
#14391=CARTESIAN_POINT('',(-0.144337567297407,-0.96,0.25));
#14392=CARTESIAN_POINT('Origin',(0.288675134594813,-0.6,0.));
#14393=CARTESIAN_POINT('',(0.144337567297406,-0.6,0.25));
#14394=CARTESIAN_POINT('',(0.144337567297406,-0.96,0.25));
#14395=CARTESIAN_POINT('Origin',(0.,-0.6,0.));
#14396=CARTESIAN_POINT('Origin',(0.,-0.96,0.));
#14445=UNCERTAINTY_MEASURE_WITH_UNIT(LENGTH_MEASURE(0.001),#14479,
'DISTANCE_ACCURACY_VALUE',
'Maximum model space distance between geometric entities at asserted c
onnectivities');
#14446=UNCERTAINTY_MEASURE_WITH_UNIT(LENGTH_MEASURE(0.001),#14479,
'DISTANCE_ACCURACY_VALUE',
'Maximum model space distance between geometric entities at asserted c
onnectivities');
#14477=(
GEOMETRIC_REPRESENTATION_CONTEXT(3)
GLOBAL_UNCERTAINTY_ASSIGNED_CONTEXT((#14445))
GLOBAL_UNIT_ASSIGNED_CONTEXT((#14479,#14481,#14482))
REPRESENTATION_CONTEXT('','3D')
);
#14478=(
GEOMETRIC_REPRESENTATION_CONTEXT(3)
GLOBAL_UNCERTAINTY_ASSIGNED_CONTEXT((#14446))
GLOBAL_UNIT_ASSIGNED_CONTEXT((#14479,#14481,#14482))
REPRESENTATION_CONTEXT('','3D')
);
#14479=(
LENGTH_UNIT()
NAMED_UNIT(*)
SI_UNIT(.CENTI.,.METRE.)
);
#14481=(
NAMED_UNIT(*)
PLANE_ANGLE_UNIT()
SI_UNIT($,.RADIAN.)
);
#14482=(
NAMED_UNIT(*)
SI_UNIT($,.STERADIAN.)
SOLID_ANGLE_UNIT()
);
#14513=SHAPE_DEFINITION_REPRESENTATION(#14584,#14633);
#14584=PRODUCT_DEFINITION_SHAPE('',$,#14665);
#14633=SHAPE_REPRESENTATION('',(#9577),#14477);
#14634=PRODUCT_DEFINITION_CONTEXT('part definition',#14729,'design');
#14665=PRODUCT_DEFINITION('Cap Screw - M6x25','Cap Screw - M6x25',#14696,
#14634);
#14696=PRODUCT_DEFINITION_FORMATION('',$,#14761);
#14729=APPLICATION_CONTEXT(
'Core Data for Automotive Mechanical Design Process');
#14730=PRODUCT_CONTEXT('part definition',#14729,'mechanical');
#14761=PRODUCT('Cap Screw - M6x25','Cap Screw - M6x25',
'Cap Screw - M6x25',(#14730));
#14832=COLOUR_RGB('Black',0.12,0.14,0.17);
#14833=FILL_AREA_STYLE_COLOUR('',#14832);
#14834=FILL_AREA_STYLE('',(#14833));
#14835=SURFACE_STYLE_FILL_AREA(#14834);
#14836=SURFACE_SIDE_STYLE('',(#14835));
#14837=SURFACE_STYLE_USAGE(.BOTH.,#14836);
#14838=PRESENTATION_STYLE_ASSIGNMENT((#14837));
ENDSEC;
END-ISO-10303-21;
